ISO-10303-21;
HEADER;
/* Generated by software containing ST-Developer
 * from STEP Tools, Inc. (www.steptools.com) 
 */

FILE_DESCRIPTION(
/* description */ ('Worm-less right-angle friction wheel drive'),
/* implementation_level */ '2;1');

FILE_NAME(
/* name */ 'Rear spring shoe (1).step',
/* time_stamp */ '2026-10-28T03:22:36-07:00',
/* author */ (''),
/* organization */ (''),
/* preprocessor_version */ 'ST-DEVELOPER v20.2',
/* originating_system */ 'Autodesk Translation Framework v15.17.0.0',
/* authorisation */ '');

FILE_SCHEMA (('AUTOMOTIVE_DESIGN { 1 0 10303 214 3 1 1 }'));
ENDSEC;

DATA;
#10=MECHANICAL_DESIGN_GEOMETRIC_PRESENTATION_REPRESENTATION('',(#632),#17046);
#538=SHAPE_REPRESENTATION_RELATIONSHIP('SRR','None',#17281,#585);
#585=ADVANCED_BREP_SHAPE_REPRESENTATION('',(#686),#17017);
#632=STYLED_ITEM('',(#17591),#686);
#686=MANIFOLD_SOLID_BREP('Body1',#8187);
#1064=PLANE('',#9228);
#1065=PLANE('',#9229);
#1436=FACE_OUTER_BOUND('',#2092,.T.);
#1437=FACE_OUTER_BOUND('',#2093,.T.);
#1438=FACE_OUTER_BOUND('',#2094,.T.);
#2092=EDGE_LOOP('',(#6590,#6591,#6592,#6593));
#2093=EDGE_LOOP('',(#6594));
#2094=EDGE_LOOP('',(#6595));
#2672=LINE('',#14422,#3212);
#3212=VECTOR('',#11038,0.7);
#3689=CIRCLE('',#9226,0.7);
#3690=CIRCLE('',#9227,0.7);
#4221=VERTEX_POINT('',#14419);
#4222=VERTEX_POINT('',#14421);
#5064=EDGE_CURVE('',#4221,#4221,#3689,.T.);
#5065=EDGE_CURVE('',#4221,#4222,#2672,.T.);
#5066=EDGE_CURVE('',#4222,#4222,#3690,.T.);
#6590=ORIENTED_EDGE('',*,*,#5064,.F.);
#6591=ORIENTED_EDGE('',*,*,#5065,.T.);
#6592=ORIENTED_EDGE('',*,*,#5066,.T.);
#6593=ORIENTED_EDGE('',*,*,#5065,.F.);
#6594=ORIENTED_EDGE('',*,*,#5064,.T.);
#6595=ORIENTED_EDGE('',*,*,#5066,.F.);
#7645=CYLINDRICAL_SURFACE('',#9225,0.7);
#7928=ADVANCED_FACE('',(#1436),#7645,.T.);
#7929=ADVANCED_FACE('',(#1437),#1064,.T.);
#7930=ADVANCED_FACE('',(#1438),#1065,.F.);
#8187=CLOSED_SHELL('',(#7928,#7929,#7930));
#9224=AXIS2_PLACEMENT_3D('',#14417,#11032,#11033);
#9225=AXIS2_PLACEMENT_3D('',#14418,#11034,#11035);
#9226=AXIS2_PLACEMENT_3D('',#14420,#11036,#11037);
#9227=AXIS2_PLACEMENT_3D('',#14423,#11039,#11040);
#9228=AXIS2_PLACEMENT_3D('',#14424,#11041,#11042);
#9229=AXIS2_PLACEMENT_3D('',#14425,#11043,#11044);
#11032=DIRECTION('axis',(0.,0.,1.));
#11033=DIRECTION('refdir',(1.,0.,0.));
#11034=DIRECTION('center_axis',(0.,1.,0.));
#11035=DIRECTION('ref_axis',(1.,0.,0.));
#11036=DIRECTION('center_axis',(0.,1.,0.));
#11037=DIRECTION('ref_axis',(1.,0.,0.));
#11038=DIRECTION('',(0.,-1.,0.));
#11039=DIRECTION('center_axis',(0.,1.,0.));
#11040=DIRECTION('ref_axis',(1.,0.,0.));
#11041=DIRECTION('center_axis',(0.,1.,0.));
#11042=DIRECTION('ref_axis',(1.,0.,0.));
#11043=DIRECTION('center_axis',(0.,1.,0.));
#11044=DIRECTION('ref_axis',(1.,0.,0.));
#14417=CARTESIAN_POINT('',(0.,0.,0.));
#14418=CARTESIAN_POINT('Origin',(5.5,7.1,4.));
#14419=CARTESIAN_POINT('',(4.8,7.4,4.));
#14420=CARTESIAN_POINT('Origin',(5.5,7.4,4.));
#14421=CARTESIAN_POINT('',(4.8,7.1,4.));
#14422=CARTESIAN_POINT('',(4.8,7.1,4.));
#14423=CARTESIAN_POINT('Origin',(5.5,7.1,4.));
#14424=CARTESIAN_POINT('Origin',(5.5,7.4,4.));
#14425=CARTESIAN_POINT('Origin',(5.5,7.1,4.));
#16964=UNCERTAINTY_MEASURE_WITH_UNIT(LENGTH_MEASURE(0.001),#17047,
'DISTANCE_ACCURACY_VALUE',
'Maximum model space distance between geometric entities at asserted c
onnectivities');
#16993=UNCERTAINTY_MEASURE_WITH_UNIT(LENGTH_MEASURE(0.001),#17047,
'DISTANCE_ACCURACY_VALUE',
'Maximum model space distance between geometric entities at asserted c
onnectivities');
#17017=(
GEOMETRIC_REPRESENTATION_CONTEXT(3)
GLOBAL_UNCERTAINTY_ASSIGNED_CONTEXT((#16964))
GLOBAL_UNIT_ASSIGNED_CONTEXT((#17047,#17049,#17050))
REPRESENTATION_CONTEXT('','3D')
);
#17046=(
GEOMETRIC_REPRESENTATION_CONTEXT(3)
GLOBAL_UNCERTAINTY_ASSIGNED_CONTEXT((#16993))
GLOBAL_UNIT_ASSIGNED_CONTEXT((#17047,#17049,#17050))
REPRESENTATION_CONTEXT('','3D')
);
#17047=(
LENGTH_UNIT()
NAMED_UNIT(*)
SI_UNIT(.CENTI.,.METRE.)
);
#17049=(
NAMED_UNIT(*)
PLANE_ANGLE_UNIT()
SI_UNIT($,.RADIAN.)
);
#17050=(
NAMED_UNIT(*)
SI_UNIT($,.STERADIAN.)
SOLID_ANGLE_UNIT()
);
#17074=SHAPE_DEFINITION_REPRESENTATION(#17126,#17281);
#17126=PRODUCT_DEFINITION_SHAPE('',$,#17334);
#17281=SHAPE_REPRESENTATION('',(#9224),#17017);
#17310=PRODUCT_DEFINITION_CONTEXT('part definition',#17468,'design');
#17334=PRODUCT_DEFINITION('Rear spring shoe (1)','Rear spring shoe (1)',#17386,
#17310);
#17386=PRODUCT_DEFINITION_FORMATION('',$,#17493);
#17468=APPLICATION_CONTEXT(
'Core Data for Automotive Mechanical Design Process');
#17469=PRODUCT_CONTEXT('part definition',#17468,'mechanical');
#17493=PRODUCT('Rear spring shoe (1)','Rear spring shoe (1)',
'Rear spring shoe (1)',(#17469));
#17585=COLOUR_RGB('Grey',0.48,0.52,0.57);
#17586=FILL_AREA_STYLE_COLOUR('',#17585);
#17587=FILL_AREA_STYLE('',(#17586));
#17588=SURFACE_STYLE_FILL_AREA(#17587);
#17589=SURFACE_SIDE_STYLE('',(#17588));
#17590=SURFACE_STYLE_USAGE(.BOTH.,#17589);
#17591=PRESENTATION_STYLE_ASSIGNMENT((#17590));
ENDSEC;
END-ISO-10303-21;
